ISO-10303-21;
HEADER;
/* Generated by software containing ST-Developer
 * from STEP Tools, Inc. (www.steptools.com) 
 */

FILE_DESCRIPTION(
/* description */ ('Rotary union on bearing shaft'),
/* implementation_level */ '2;1');

FILE_NAME(
/* name */ 'Seal gland (1).step',
/* time_stamp */ '2026-10-28T03:24:01-07:00',
/* author */ (''),
/* organization */ (''),
/* preprocessor_version */ 'ST-DEVELOPER v20.2',
/* originating_system */ 'Autodesk Translation Framework v15.17.0.0',
/* authorisation */ '');

FILE_SCHEMA (('AUTOMOTIVE_DESIGN { 1 0 10303 214 3 1 1 }'));
ENDSEC;

DATA;
#10=MECHANICAL_DESIGN_GEOMETRIC_PRESENTATION_REPRESENTATION('',(#317),#9448);
#263=SHAPE_REPRESENTATION_RELATIONSHIP('SRR','None',#9563,#290);
#290=ADVANCED_BREP_SHAPE_REPRESENTATION('',(#352),#9423);
#317=STYLED_ITEM('',(#9785),#352);
#352=MANIFOLD_SOLID_BREP('Body1',#4872);
#414=FACE_BOUND('',#1053,.T.);
#415=FACE_BOUND('',#1055,.T.);
#416=FACE_BOUND('',#1060,.T.);
#417=FACE_BOUND('',#1062,.T.);
#525=PLANE('',#5330);
#526=PLANE('',#5332);
#527=PLANE('',#5341);
#528=PLANE('',#5342);
#718=FACE_OUTER_BOUND('',#1051,.T.);
#719=FACE_OUTER_BOUND('',#1052,.T.);
#720=FACE_OUTER_BOUND('',#1054,.T.);
#721=FACE_OUTER_BOUND('',#1056,.T.);
#722=FACE_OUTER_BOUND('',#1057,.T.);
#723=FACE_OUTER_BOUND('',#1058,.T.);
#724=FACE_OUTER_BOUND('',#1059,.T.);
#725=FACE_OUTER_BOUND('',#1061,.T.);
#1051=EDGE_LOOP('',(#3525,#3526,#3527,#3528));
#1052=EDGE_LOOP('',(#3529));
#1053=EDGE_LOOP('',(#3530));
#1054=EDGE_LOOP('',(#3531));
#1055=EDGE_LOOP('',(#3532));
#1056=EDGE_LOOP('',(#3533,#3534,#3535,#3536));
#1057=EDGE_LOOP('',(#3537,#3538,#3539,#3540));
#1058=EDGE_LOOP('',(#3541,#3542,#3543,#3544));
#1059=EDGE_LOOP('',(#3545));
#1060=EDGE_LOOP('',(#3546));
#1061=EDGE_LOOP('',(#3547));
#1062=EDGE_LOOP('',(#3548));
#1432=LINE('',#7751,#1752);
#1433=LINE('',#7761,#1753);
#1434=LINE('',#7766,#1754);
#1435=LINE('',#7771,#1755);
#1752=VECTOR('',#6149,1.16);
#1753=VECTOR('',#6162,1.005);
#1754=VECTOR('',#6169,1.005);
#1755=VECTOR('',#6174,2.34);
#2055=CIRCLE('',#5328,1.16);
#2056=CIRCLE('',#5329,1.16);
#2057=CIRCLE('',#5331,1.005);
#2058=CIRCLE('',#5333,1.005);
#2059=CIRCLE('',#5335,1.005);
#2060=CIRCLE('',#5337,1.005);
#2061=CIRCLE('',#5339,2.34);
#2062=CIRCLE('',#5340,2.34);
#2338=VERTEX_POINT('',#7748);
#2339=VERTEX_POINT('',#7750);
#2340=VERTEX_POINT('',#7754);
#2341=VERTEX_POINT('',#7757);
#2342=VERTEX_POINT('',#7760);
#2343=VERTEX_POINT('',#7764);
#2344=VERTEX_POINT('',#7768);
#2345=VERTEX_POINT('',#7770);
#2790=EDGE_CURVE('',#2338,#2338,#2055,.T.);
#2791=EDGE_CURVE('',#2338,#2339,#1432,.T.);
#2792=EDGE_CURVE('',#2339,#2339,#2056,.T.);
#2793=EDGE_CURVE('',#2340,#2340,#2057,.T.);
#2794=EDGE_CURVE('',#2341,#2341,#2058,.T.);
#2795=EDGE_CURVE('',#2341,#2342,#1433,.T.);
#2796=EDGE_CURVE('',#2342,#2342,#2059,.T.);
#2797=EDGE_CURVE('',#2343,#2343,#2060,.T.);
#2798=EDGE_CURVE('',#2343,#2340,#1434,.T.);
#2799=EDGE_CURVE('',#2344,#2344,#2061,.T.);
#2800=EDGE_CURVE('',#2344,#2345,#1435,.T.);
#2801=EDGE_CURVE('',#2345,#2345,#2062,.T.);
#3525=ORIENTED_EDGE('',*,*,#2790,.F.);
#3526=ORIENTED_EDGE('',*,*,#2791,.T.);
#3527=ORIENTED_EDGE('',*,*,#2792,.T.);
#3528=ORIENTED_EDGE('',*,*,#2791,.F.);
#3529=ORIENTED_EDGE('',*,*,#2792,.F.);
#3530=ORIENTED_EDGE('',*,*,#2793,.F.);
#3531=ORIENTED_EDGE('',*,*,#2790,.T.);
#3532=ORIENTED_EDGE('',*,*,#2794,.F.);
#3533=ORIENTED_EDGE('',*,*,#2794,.T.);
#3534=ORIENTED_EDGE('',*,*,#2795,.T.);
#3535=ORIENTED_EDGE('',*,*,#2796,.T.);
#3536=ORIENTED_EDGE('',*,*,#2795,.F.);
#3537=ORIENTED_EDGE('',*,*,#2797,.F.);
#3538=ORIENTED_EDGE('',*,*,#2798,.T.);
#3539=ORIENTED_EDGE('',*,*,#2793,.T.);
#3540=ORIENTED_EDGE('',*,*,#2798,.F.);
#3541=ORIENTED_EDGE('',*,*,#2799,.F.);
#3542=ORIENTED_EDGE('',*,*,#2800,.T.);
#3543=ORIENTED_EDGE('',*,*,#2801,.T.);
#3544=ORIENTED_EDGE('',*,*,#2800,.F.);
#3545=ORIENTED_EDGE('',*,*,#2799,.T.);
#3546=ORIENTED_EDGE('',*,*,#2797,.T.);
#3547=ORIENTED_EDGE('',*,*,#2801,.F.);
#3548=ORIENTED_EDGE('',*,*,#2796,.F.);
#4502=CYLINDRICAL_SURFACE('',#5327,1.16);
#4503=CYLINDRICAL_SURFACE('',#5334,1.005);
#4504=CYLINDRICAL_SURFACE('',#5336,1.005);
#4505=CYLINDRICAL_SURFACE('',#5338,2.34);
#4631=ADVANCED_FACE('',(#718),#4502,.F.);
#4632=ADVANCED_FACE('',(#719,#414),#525,.F.);
#4633=ADVANCED_FACE('',(#720,#415),#526,.T.);
#4634=ADVANCED_FACE('',(#721),#4503,.F.);
#4635=ADVANCED_FACE('',(#722),#4504,.F.);
#4636=ADVANCED_FACE('',(#723),#4505,.T.);
#4637=ADVANCED_FACE('',(#724,#416),#527,.T.);
#4638=ADVANCED_FACE('',(#725,#417),#528,.F.);
#4872=CLOSED_SHELL('',(#4631,#4632,#4633,#4634,#4635,#4636,#4637,#4638));
#5326=AXIS2_PLACEMENT_3D('',#7746,#6143,#6144);
#5327=AXIS2_PLACEMENT_3D('',#7747,#6145,#6146);
#5328=AXIS2_PLACEMENT_3D('',#7749,#6147,#6148);
#5329=AXIS2_PLACEMENT_3D('',#7752,#6150,#6151);
#5330=AXIS2_PLACEMENT_3D('',#7753,#6152,#6153);
#5331=AXIS2_PLACEMENT_3D('',#7755,#6154,#6155);
#5332=AXIS2_PLACEMENT_3D('',#7756,#6156,#6157);
#5333=AXIS2_PLACEMENT_3D('',#7758,#6158,#6159);
#5334=AXIS2_PLACEMENT_3D('',#7759,#6160,#6161);
#5335=AXIS2_PLACEMENT_3D('',#7762,#6163,#6164);
#5336=AXIS2_PLACEMENT_3D('',#7763,#6165,#6166);
#5337=AXIS2_PLACEMENT_3D('',#7765,#6167,#6168);
#5338=AXIS2_PLACEMENT_3D('',#7767,#6170,#6171);
#5339=AXIS2_PLACEMENT_3D('',#7769,#6172,#6173);
#5340=AXIS2_PLACEMENT_3D('',#7772,#6175,#6176);
#5341=AXIS2_PLACEMENT_3D('',#7773,#6177,#6178);
#5342=AXIS2_PLACEMENT_3D('',#7774,#6179,#6180);
#6143=DIRECTION('axis',(0.,0.,1.));
#6144=DIRECTION('refdir',(1.,0.,0.));
#6145=DIRECTION('center_axis',(0.,1.,0.));
#6146=DIRECTION('ref_axis',(1.,0.,0.));
#6147=DIRECTION('center_axis',(0.,1.,0.));
#6148=DIRECTION('ref_axis',(1.,0.,0.));
#6149=DIRECTION('',(0.,1.,0.));
#6150=DIRECTION('center_axis',(0.,1.,0.));
#6151=DIRECTION('ref_axis',(1.,0.,0.));
#6152=DIRECTION('center_axis',(0.,1.,0.));
#6153=DIRECTION('ref_axis',(1.,0.,0.));
#6154=DIRECTION('center_axis',(0.,-1.,0.));
#6155=DIRECTION('ref_axis',(1.,0.,0.));
#6156=DIRECTION('center_axis',(0.,1.,0.));
#6157=DIRECTION('ref_axis',(1.,0.,0.));
#6158=DIRECTION('center_axis',(0.,1.,0.));
#6159=DIRECTION('ref_axis',(1.,0.,0.));
#6160=DIRECTION('center_axis',(0.,1.,0.));
#6161=DIRECTION('ref_axis',(1.,0.,0.));
#6162=DIRECTION('',(0.,-1.,0.));
#6163=DIRECTION('center_axis',(0.,-1.,0.));
#6164=DIRECTION('ref_axis',(1.,0.,0.));
#6165=DIRECTION('center_axis',(0.,1.,0.));
#6166=DIRECTION('ref_axis',(1.,0.,0.));
#6167=DIRECTION('center_axis',(0.,-1.,0.));
#6168=DIRECTION('ref_axis',(1.,0.,0.));
#6169=DIRECTION('',(0.,-1.,0.));
#6170=DIRECTION('center_axis',(0.,1.,0.));
#6171=DIRECTION('ref_axis',(1.,0.,0.));
#6172=DIRECTION('center_axis',(0.,1.,0.));
#6173=DIRECTION('ref_axis',(1.,0.,0.));
#6174=DIRECTION('',(0.,-1.,0.));
#6175=DIRECTION('center_axis',(0.,1.,0.));
#6176=DIRECTION('ref_axis',(1.,0.,0.));
#6177=DIRECTION('center_axis',(0.,1.,0.));
#6178=DIRECTION('ref_axis',(1.,0.,0.));
#6179=DIRECTION('center_axis',(0.,1.,0.));
#6180=DIRECTION('ref_axis',(1.,0.,0.));
#7746=CARTESIAN_POINT('',(0.,0.,0.));
#7747=CARTESIAN_POINT('Origin',(0.,3.8,4.5));
#7748=CARTESIAN_POINT('',(-1.16,3.8,4.5));
#7749=CARTESIAN_POINT('Origin',(0.,3.8,4.5));
#7750=CARTESIAN_POINT('',(-1.16,4.1,4.5));
#7751=CARTESIAN_POINT('',(-1.16,3.8,4.5));
#7752=CARTESIAN_POINT('Origin',(0.,4.1,4.5));
#7753=CARTESIAN_POINT('Origin',(0.,4.1,4.5));
#7754=CARTESIAN_POINT('',(-1.005,4.1,4.5));
#7755=CARTESIAN_POINT('Origin',(0.,4.1,4.5));
#7756=CARTESIAN_POINT('Origin',(0.,3.8,4.5));
#7757=CARTESIAN_POINT('',(-1.005,3.8,4.5));
#7758=CARTESIAN_POINT('Origin',(0.,3.8,4.5));
#7759=CARTESIAN_POINT('Origin',(0.,3.6,4.5));
#7760=CARTESIAN_POINT('',(-1.005,3.6,4.5));
#7761=CARTESIAN_POINT('',(-1.005,3.6,4.5));
#7762=CARTESIAN_POINT('Origin',(0.,3.6,4.5));
#7763=CARTESIAN_POINT('Origin',(0.,3.6,4.5));
#7764=CARTESIAN_POINT('',(-1.005,4.3,4.5));
#7765=CARTESIAN_POINT('Origin',(0.,4.3,4.5));
#7766=CARTESIAN_POINT('',(-1.005,3.6,4.5));
#7767=CARTESIAN_POINT('Origin',(0.,3.6,4.5));
#7768=CARTESIAN_POINT('',(-2.34,4.3,4.5));
#7769=CARTESIAN_POINT('Origin',(0.,4.3,4.5));
#7770=CARTESIAN_POINT('',(-2.34,3.6,4.5));
#7771=CARTESIAN_POINT('',(-2.34,3.6,4.5));
#7772=CARTESIAN_POINT('Origin',(0.,3.6,4.5));
#7773=CARTESIAN_POINT('Origin',(0.,4.3,4.5));
#7774=CARTESIAN_POINT('Origin',(0.,3.6,4.5));
#9391=UNCERTAINTY_MEASURE_WITH_UNIT(LENGTH_MEASURE(0.001),#9449,
'DISTANCE_ACCURACY_VALUE',
'Maximum model space distance between geometric entities at asserted c
onnectivities');
#9416=UNCERTAINTY_MEASURE_WITH_UNIT(LENGTH_MEASURE(0.001),#9449,
'DISTANCE_ACCURACY_VALUE',
'Maximum model space distance between geometric entities at asserted c
onnectivities');
#9423=(
GEOMETRIC_REPRESENTATION_CONTEXT(3)
GLOBAL_UNCERTAINTY_ASSIGNED_CONTEXT((#9391))
GLOBAL_UNIT_ASSIGNED_CONTEXT((#9449,#9451,#9452))
REPRESENTATION_CONTEXT('','3D')
);
#9448=(
GEOMETRIC_REPRESENTATION_CONTEXT(3)
GLOBAL_UNCERTAINTY_ASSIGNED_CONTEXT((#9416))
GLOBAL_UNIT_ASSIGNED_CONTEXT((#9449,#9451,#9452))
REPRESENTATION_CONTEXT('','3D')
);
#9449=(
LENGTH_UNIT()
NAMED_UNIT(*)
SI_UNIT(.CENTI.,.METRE.)
);
#9451=(
NAMED_UNIT(*)
PLANE_ANGLE_UNIT()
SI_UNIT($,.RADIAN.)
);
#9452=(
NAMED_UNIT(*)
SI_UNIT($,.STERADIAN.)
SOLID_ANGLE_UNIT()
);
#9459=SHAPE_DEFINITION_REPRESENTATION(#9490,#9563);
#9490=PRODUCT_DEFINITION_SHAPE('',$,#9595);
#9563=SHAPE_REPRESENTATION('',(#5326),#9423);
#9588=PRODUCT_DEFINITION_CONTEXT('part definition',#9683,'design');
#9595=PRODUCT_DEFINITION('Seal gland (1)','Seal gland (1)',#9626,#9588);
#9626=PRODUCT_DEFINITION_FORMATION('',$,#9691);
#9683=APPLICATION_CONTEXT(
'Core Data for Automotive Mechanical Design Process');
#9684=PRODUCT_CONTEXT('part definition',#9683,'mechanical');
#9691=PRODUCT('Seal gland (1)','Seal gland (1)','Seal gland (1)',(#9684));
#9779=COLOUR_RGB('Black',0.12,0.14,0.17);
#9780=FILL_AREA_STYLE_COLOUR('',#9779);
#9781=FILL_AREA_STYLE('',(#9780));
#9782=SURFACE_STYLE_FILL_AREA(#9781);
#9783=SURFACE_SIDE_STYLE('',(#9782));
#9784=SURFACE_STYLE_USAGE(.BOTH.,#9783);
#9785=PRESENTATION_STYLE_ASSIGNMENT((#9784));
ENDSEC;
END-ISO-10303-21;
